ISO-10303-21;
HEADER;
/* Generated by software containing ST-Developer
 * from STEP Tools, Inc. (www.steptools.com) 
 */

FILE_DESCRIPTION(
/* description */ ('Belt tension measurement rig'),
/* implementation_level */ '2;1');

FILE_NAME(
/* name */ 'Socket Set Screw - M4x6.step',
/* time_stamp */ '2026-10-28T03:24:44-07:00',
/* author */ (''),
/* organization */ (''),
/* preprocessor_version */ 'ST-DEVELOPER v20.2',
/* originating_system */ 'Autodesk Translation Framework v15.17.0.0',
/* authorisation */ '');

FILE_SCHEMA (('AUTOMOTIVE_DESIGN { 1 0 10303 214 3 1 1 }'));
ENDSEC;

DATA;
#10=MECHANICAL_DESIGN_GEOMETRIC_PRESENTATION_REPRESENTATION('',(#761),#23587);
#485=CONICAL_SURFACE('',#14472,0.185,0.785398163397449);
#486=CONICAL_SURFACE('',#14476,0.1625,0.785398163397449);
#636=SHAPE_REPRESENTATION_RELATIONSHIP('SRR','None',#23888,#691);
#691=ADVANCED_BREP_SHAPE_REPRESENTATION('',(#828),#23586);
#761=STYLED_ITEM('',(#24218),#828);
#828=MANIFOLD_SOLID_BREP('Body1',#12269);
#1036=FACE_BOUND('',#2963,.T.);
#1343=PLANE('',#14463);
#1344=PLANE('',#14464);
#1345=PLANE('',#14465);
#1346=PLANE('',#14466);
#1347=PLANE('',#14467);
#1348=PLANE('',#14468);
#1349=PLANE('',#14469);
#1350=PLANE('',#14470);
#1351=PLANE('',#14478);
#2044=FACE_OUTER_BOUND('',#2955,.T.);
#2045=FACE_OUTER_BOUND('',#2956,.T.);
#2046=FACE_OUTER_BOUND('',#2957,.T.);
#2047=FACE_OUTER_BOUND('',#2958,.T.);
#2048=FACE_OUTER_BOUND('',#2959,.T.);
#2049=FACE_OUTER_BOUND('',#2960,.T.);
#2050=FACE_OUTER_BOUND('',#2961,.T.);
#2051=FACE_OUTER_BOUND('',#2962,.T.);
#2052=FACE_OUTER_BOUND('',#2964,.T.);
#2053=FACE_OUTER_BOUND('',#2965,.T.);
#2054=FACE_OUTER_BOUND('',#2966,.T.);
#2055=FACE_OUTER_BOUND('',#2967,.T.);
#2955=EDGE_LOOP('',(#11108,#11109,#11110,#11111));
#2956=EDGE_LOOP('',(#11112,#11113,#11114,#11115));
#2957=EDGE_LOOP('',(#11116,#11117,#11118,#11119));
#2958=EDGE_LOOP('',(#11120,#11121,#11122,#11123));
#2959=EDGE_LOOP('',(#11124,#11125,#11126,#11127));
#2960=EDGE_LOOP('',(#11128,#11129,#11130,#11131));
#2961=EDGE_LOOP('',(#11132,#11133,#11134,#11135,#11136,#11137));
#2962=EDGE_LOOP('',(#11138));
#2963=EDGE_LOOP('',(#11139,#11140,#11141,#11142,#11143,#11144));
#2964=EDGE_LOOP('',(#11145,#11146,#11147,#11148));
#2965=EDGE_LOOP('',(#11149,#11150,#11151,#11152));
#2966=EDGE_LOOP('',(#11153,#11154,#11155,#11156));
#2967=EDGE_LOOP('',(#11157));
#3698=LINE('',#23370,#4449);
#3699=LINE('',#23372,#4450);
#3700=LINE('',#23374,#4451);
#3701=LINE('',#23375,#4452);
#3702=LINE('',#23378,#4453);
#3703=LINE('',#23380,#4454);
#3704=LINE('',#23381,#4455);
#3705=LINE('',#23384,#4456);
#3706=LINE('',#23386,#4457);
#3707=LINE('',#23387,#4458);
#3708=LINE('',#23390,#4459);
#3709=LINE('',#23392,#4460);
#3710=LINE('',#23393,#4461);
#3711=LINE('',#23396,#4462);
#3712=LINE('',#23398,#4463);
#3713=LINE('',#23399,#4464);
#3714=LINE('',#23401,#4465);
#3715=LINE('',#23402,#4466);
#3716=LINE('',#23410,#4467);
#3717=LINE('',#23414,#4468);
#3718=LINE('',#23418,#4469);
#4449=VECTOR('',#18423,1.);
#4450=VECTOR('',#18424,1.);
#4451=VECTOR('',#18425,1.);
#4452=VECTOR('',#18426,1.);
#4453=VECTOR('',#18429,1.);
#4454=VECTOR('',#18430,1.);
#4455=VECTOR('',#18431,1.);
#4456=VECTOR('',#18434,1.);
#4457=VECTOR('',#18435,1.);
#4458=VECTOR('',#18436,1.);
#4459=VECTOR('',#18439,1.);
#4460=VECTOR('',#18440,1.);
#4461=VECTOR('',#18441,1.);
#4462=VECTOR('',#18444,1.);
#4463=VECTOR('',#18445,1.);
#4464=VECTOR('',#18446,1.);
#4465=VECTOR('',#18449,1.);
#4466=VECTOR('',#18450,1.);
#4467=VECTOR('',#18461,0.185);
#4468=VECTOR('',#18466,0.2);
#4469=VECTOR('',#18471,0.1625);
#5234=CIRCLE('',#14471,0.17);
#5235=CIRCLE('',#14473,0.1954);
#5236=CIRCLE('',#14475,0.1954);
#5237=CIRCLE('',#14477,0.125);
#6312=VERTEX_POINT('',#23368);
#6313=VERTEX_POINT('',#23369);
#6314=VERTEX_POINT('',#23371);
#6315=VERTEX_POINT('',#23373);
#6316=VERTEX_POINT('',#23377);
#6317=VERTEX_POINT('',#23379);
#6318=VERTEX_POINT('',#23383);
#6319=VERTEX_POINT('',#23385);
#6320=VERTEX_POINT('',#23389);
#6321=VERTEX_POINT('',#23391);
#6322=VERTEX_POINT('',#23395);
#6323=VERTEX_POINT('',#23397);
#6324=VERTEX_POINT('',#23405);
#6325=VERTEX_POINT('',#23408);
#6326=VERTEX_POINT('',#23412);
#6327=VERTEX_POINT('',#23416);
#7913=EDGE_CURVE('',#6312,#6313,#3698,.T.);
#7914=EDGE_CURVE('',#6312,#6314,#3699,.T.);
#7915=EDGE_CURVE('',#6314,#6315,#3700,.T.);
#7916=EDGE_CURVE('',#6313,#6315,#3701,.T.);
#7917=EDGE_CURVE('',#6316,#6312,#3702,.T.);
#7918=EDGE_CURVE('',#6316,#6317,#3703,.T.);
#7919=EDGE_CURVE('',#6317,#6314,#3704,.T.);
#7920=EDGE_CURVE('',#6318,#6316,#3705,.T.);
#7921=EDGE_CURVE('',#6318,#6319,#3706,.T.);
#7922=EDGE_CURVE('',#6319,#6317,#3707,.T.);
#7923=EDGE_CURVE('',#6320,#6318,#3708,.T.);
#7924=EDGE_CURVE('',#6320,#6321,#3709,.T.);
#7925=EDGE_CURVE('',#6321,#6319,#3710,.T.);
#7926=EDGE_CURVE('',#6322,#6320,#3711,.T.);
#7927=EDGE_CURVE('',#6322,#6323,#3712,.T.);
#7928=EDGE_CURVE('',#6323,#6321,#3713,.T.);
#7929=EDGE_CURVE('',#6313,#6322,#3714,.T.);
#7930=EDGE_CURVE('',#6315,#6323,#3715,.T.);
#7931=EDGE_CURVE('',#6324,#6324,#5234,.T.);
#7932=EDGE_CURVE('',#6325,#6325,#5235,.T.);
#7933=EDGE_CURVE('',#6325,#6324,#3716,.T.);
#7934=EDGE_CURVE('',#6326,#6326,#5236,.F.);
#7935=EDGE_CURVE('',#6326,#6325,#3717,.T.);
#7936=EDGE_CURVE('',#6327,#6327,#5237,.T.);
#7937=EDGE_CURVE('',#6327,#6326,#3718,.T.);
#11108=ORIENTED_EDGE('',*,*,#7913,.F.);
#11109=ORIENTED_EDGE('',*,*,#7914,.T.);
#11110=ORIENTED_EDGE('',*,*,#7915,.T.);
#11111=ORIENTED_EDGE('',*,*,#7916,.F.);
#11112=ORIENTED_EDGE('',*,*,#7917,.F.);
#11113=ORIENTED_EDGE('',*,*,#7918,.T.);
#11114=ORIENTED_EDGE('',*,*,#7919,.T.);
#11115=ORIENTED_EDGE('',*,*,#7914,.F.);
#11116=ORIENTED_EDGE('',*,*,#7920,.F.);
#11117=ORIENTED_EDGE('',*,*,#7921,.T.);
#11118=ORIENTED_EDGE('',*,*,#7922,.T.);
#11119=ORIENTED_EDGE('',*,*,#7918,.F.);
#11120=ORIENTED_EDGE('',*,*,#7923,.F.);
#11121=ORIENTED_EDGE('',*,*,#7924,.T.);
#11122=ORIENTED_EDGE('',*,*,#7925,.T.);
#11123=ORIENTED_EDGE('',*,*,#7921,.F.);
#11124=ORIENTED_EDGE('',*,*,#7926,.F.);
#11125=ORIENTED_EDGE('',*,*,#7927,.T.);
#11126=ORIENTED_EDGE('',*,*,#7928,.T.);
#11127=ORIENTED_EDGE('',*,*,#7924,.F.);
#11128=ORIENTED_EDGE('',*,*,#7929,.F.);
#11129=ORIENTED_EDGE('',*,*,#7916,.T.);
#11130=ORIENTED_EDGE('',*,*,#7930,.T.);
#11131=ORIENTED_EDGE('',*,*,#7927,.F.);
#11132=ORIENTED_EDGE('',*,*,#7930,.F.);
#11133=ORIENTED_EDGE('',*,*,#7915,.F.);
#11134=ORIENTED_EDGE('',*,*,#7919,.F.);
#11135=ORIENTED_EDGE('',*,*,#7922,.F.);
#11136=ORIENTED_EDGE('',*,*,#7925,.F.);
#11137=ORIENTED_EDGE('',*,*,#7928,.F.);
#11138=ORIENTED_EDGE('',*,*,#7931,.F.);
#11139=ORIENTED_EDGE('',*,*,#7913,.T.);
#11140=ORIENTED_EDGE('',*,*,#7929,.T.);
#11141=ORIENTED_EDGE('',*,*,#7926,.T.);
#11142=ORIENTED_EDGE('',*,*,#7923,.T.);
#11143=ORIENTED_EDGE('',*,*,#7920,.T.);
#11144=ORIENTED_EDGE('',*,*,#7917,.T.);
#11145=ORIENTED_EDGE('',*,*,#7932,.F.);
#11146=ORIENTED_EDGE('',*,*,#7933,.T.);
#11147=ORIENTED_EDGE('',*,*,#7931,.T.);
#11148=ORIENTED_EDGE('',*,*,#7933,.F.);
#11149=ORIENTED_EDGE('',*,*,#7934,.F.);
#11150=ORIENTED_EDGE('',*,*,#7935,.T.);
#11151=ORIENTED_EDGE('',*,*,#7932,.T.);
#11152=ORIENTED_EDGE('',*,*,#7935,.F.);
#11153=ORIENTED_EDGE('',*,*,#7936,.F.);
#11154=ORIENTED_EDGE('',*,*,#7937,.T.);
#11155=ORIENTED_EDGE('',*,*,#7934,.T.);
#11156=ORIENTED_EDGE('',*,*,#7937,.F.);
#11157=ORIENTED_EDGE('',*,*,#7936,.T.);
#11492=CYLINDRICAL_SURFACE('',#14474,0.1954);
#12185=ADVANCED_FACE('',(#2044),#1343,.F.);
#12186=ADVANCED_FACE('',(#2045),#1344,.F.);
#12187=ADVANCED_FACE('',(#2046),#1345,.F.);
#12188=ADVANCED_FACE('',(#2047),#1346,.F.);
#12189=ADVANCED_FACE('',(#2048),#1347,.F.);
#12190=ADVANCED_FACE('',(#2049),#1348,.F.);
#12191=ADVANCED_FACE('',(#2050),#1349,.F.);
#12192=ADVANCED_FACE('',(#2051,#1036),#1350,.T.);
#12193=ADVANCED_FACE('',(#2052),#485,.T.);
#12194=ADVANCED_FACE('',(#2053),#11492,.T.);
#12195=ADVANCED_FACE('',(#2054),#486,.T.);
#12196=ADVANCED_FACE('',(#2055),#1351,.T.);
#12269=CLOSED_SHELL('',(#12185,#12186,#12187,#12188,#12189,#12190,#12191,
#12192,#12193,#12194,#12195,#12196));
#14462=AXIS2_PLACEMENT_3D('',#23366,#18419,#18420);
#14463=AXIS2_PLACEMENT_3D('',#23367,#18421,#18422);
#14464=AXIS2_PLACEMENT_3D('',#23376,#18427,#18428);
#14465=AXIS2_PLACEMENT_3D('',#23382,#18432,#18433);
#14466=AXIS2_PLACEMENT_3D('',#23388,#18437,#18438);
#14467=AXIS2_PLACEMENT_3D('',#23394,#18442,#18443);
#14468=AXIS2_PLACEMENT_3D('',#23400,#18447,#18448);
#14469=AXIS2_PLACEMENT_3D('',#23403,#18451,#18452);
#14470=AXIS2_PLACEMENT_3D('',#23404,#18453,#18454);
#14471=AXIS2_PLACEMENT_3D('',#23406,#18455,#18456);
#14472=AXIS2_PLACEMENT_3D('',#23407,#18457,#18458);
#14473=AXIS2_PLACEMENT_3D('',#23409,#18459,#18460);
#14474=AXIS2_PLACEMENT_3D('',#23411,#18462,#18463);
#14475=AXIS2_PLACEMENT_3D('',#23413,#18464,#18465);
#14476=AXIS2_PLACEMENT_3D('',#23415,#18467,#18468);
#14477=AXIS2_PLACEMENT_3D('',#23417,#18469,#18470);
#14478=AXIS2_PLACEMENT_3D('',#23419,#18472,#18473);
#18419=DIRECTION('axis',(0.,0.,1.));
#18420=DIRECTION('refdir',(1.,0.,0.));
#18421=DIRECTION('center_axis',(0.866025403784439,0.,-0.5));
#18422=DIRECTION('ref_axis',(0.5,0.,0.866025403784439));
#18423=DIRECTION('',(0.5,0.,0.866025403784439));
#18424=DIRECTION('',(0.,-1.,0.));
#18425=DIRECTION('',(0.5,0.,0.866025403784439));
#18426=DIRECTION('',(0.,-1.,0.));
#18427=DIRECTION('center_axis',(1.20185167898973E-16,0.,-1.));
#18428=DIRECTION('ref_axis',(1.,0.,1.20185167898973E-16));
#18429=DIRECTION('',(1.,0.,1.20185167898973E-16));
#18430=DIRECTION('',(0.,-1.,0.));
#18431=DIRECTION('',(1.,0.,1.20185167898973E-16));
#18432=DIRECTION('center_axis',(-0.866025403784439,0.,-0.5));
#18433=DIRECTION('ref_axis',(0.5,0.,-0.866025403784439));
#18434=DIRECTION('',(0.5,0.,-0.866025403784439));
#18435=DIRECTION('',(0.,-1.,0.));
#18436=DIRECTION('',(0.5,0.,-0.866025403784439));
#18437=DIRECTION('center_axis',(-0.866025403784439,0.,0.5));
#18438=DIRECTION('ref_axis',(-0.5,0.,-0.866025403784439));
#18439=DIRECTION('',(-0.5,0.,-0.866025403784439));
#18440=DIRECTION('',(0.,-1.,0.));
#18441=DIRECTION('',(-0.5,0.,-0.866025403784439));
#18442=DIRECTION('center_axis',(-2.40370335797945E-16,0.,1.));
#18443=DIRECTION('ref_axis',(-1.,0.,-2.40370335797945E-16));
#18444=DIRECTION('',(-1.,0.,-2.40370335797945E-16));
#18445=DIRECTION('',(0.,-1.,0.));
#18446=DIRECTION('',(-1.,0.,-2.40370335797945E-16));
#18447=DIRECTION('center_axis',(0.866025403784439,0.,0.5));
#18448=DIRECTION('ref_axis',(-0.5,0.,0.866025403784439));
#18449=DIRECTION('',(-0.5,0.,0.866025403784439));
#18450=DIRECTION('',(-0.5,0.,0.866025403784439));
#18451=DIRECTION('center_axis',(0.,-1.,0.));
#18452=DIRECTION('ref_axis',(0.,0.,-1.));
#18453=DIRECTION('center_axis',(0.,1.,0.));
#18454=DIRECTION('ref_axis',(0.,0.,1.));
#18455=DIRECTION('center_axis',(0.,-1.,0.));
#18456=DIRECTION('ref_axis',(1.,0.,0.));
#18457=DIRECTION('center_axis',(0.,-1.,0.));
#18458=DIRECTION('ref_axis',(1.,0.,0.));
#18459=DIRECTION('center_axis',(0.,-1.,0.));
#18460=DIRECTION('ref_axis',(1.,0.,0.));
#18461=DIRECTION('',(0.707106781186548,0.707106781186547,8.65956056235494E-17));
#18462=DIRECTION('center_axis',(0.,-1.,0.));
#18463=DIRECTION('ref_axis',(1.,0.,0.));
#18464=DIRECTION('center_axis',(0.,1.,0.));
#18465=DIRECTION('ref_axis',(1.,0.,0.));
#18466=DIRECTION('',(0.,1.,0.));
#18467=DIRECTION('center_axis',(0.,1.,0.));
#18468=DIRECTION('ref_axis',(1.,0.,0.));
#18469=DIRECTION('center_axis',(0.,-1.,0.));
#18470=DIRECTION('ref_axis',(1.,0.,0.));
#18471=DIRECTION('',(-0.707106781186548,0.707106781186547,-8.65956056235494E-17));
#18472=DIRECTION('center_axis',(0.,-1.,0.));
#18473=DIRECTION('ref_axis',(0.,0.,-1.));
#23366=CARTESIAN_POINT('',(0.,0.,0.));
#23367=CARTESIAN_POINT('Origin',(0.0577350269189626,0.,-0.1));
#23368=CARTESIAN_POINT('',(0.0577350269189626,0.,-0.1));
#23369=CARTESIAN_POINT('',(0.115470053837925,0.,0.));
#23370=CARTESIAN_POINT('',(0.0934187836487032,0.,-0.0381939203391614));
#23371=CARTESIAN_POINT('',(0.0577350269189626,-0.2,-0.1));
#23372=CARTESIAN_POINT('',(0.0577350269189626,0.,-0.1));
#23373=CARTESIAN_POINT('',(0.115470053837925,-0.2,0.));
#23374=CARTESIAN_POINT('',(0.115470053837925,-0.2,0.));
#23375=CARTESIAN_POINT('',(0.115470053837925,0.,0.));
#23376=CARTESIAN_POINT('Origin',(-0.0577350269189626,0.,-0.1));
#23377=CARTESIAN_POINT('',(-0.0577350269189626,0.,-0.1));
#23378=CARTESIAN_POINT('',(0.0561324865405187,0.,-0.1));
#23379=CARTESIAN_POINT('',(-0.0577350269189626,-0.2,-0.1));
#23380=CARTESIAN_POINT('',(-0.0577350269189626,0.,-0.1));
#23381=CARTESIAN_POINT('',(0.0577350269189626,-0.2,-0.1));
#23382=CARTESIAN_POINT('Origin',(-0.115470053837925,0.,-1.38777878078145E-17));
#23383=CARTESIAN_POINT('',(-0.115470053837925,0.,-1.41410031829988E-17));
#23384=CARTESIAN_POINT('',(-0.0797862971081845,0.,-0.0618060796608387));
#23385=CARTESIAN_POINT('',(-0.115470053837925,-0.2,-1.38777878078145E-17));
#23386=CARTESIAN_POINT('',(-0.115470053837925,0.,-1.41410031829988E-17));
#23387=CARTESIAN_POINT('',(-0.0577350269189626,-0.2,-0.1));
#23388=CARTESIAN_POINT('Origin',(-0.0577350269189626,0.,0.1));
#23389=CARTESIAN_POINT('',(-0.0577350269189626,0.,0.1));
#23390=CARTESIAN_POINT('',(-0.0509187836487033,0.,0.111806079660839));
#23391=CARTESIAN_POINT('',(-0.0577350269189626,-0.2,0.1));
#23392=CARTESIAN_POINT('',(-0.0577350269189626,0.,0.1));
#23393=CARTESIAN_POINT('',(-0.115470053837925,-0.2,-1.41410031829988E-17));
#23394=CARTESIAN_POINT('Origin',(0.0577350269189626,0.,0.1));
#23395=CARTESIAN_POINT('',(0.0577350269189626,0.,0.1));
#23396=CARTESIAN_POINT('',(0.113867513459481,0.,0.1));
#23397=CARTESIAN_POINT('',(0.0577350269189626,-0.2,0.1));
#23398=CARTESIAN_POINT('',(0.0577350269189626,0.,0.1));
#23399=CARTESIAN_POINT('',(-0.0577350269189626,-0.2,0.1));
#23400=CARTESIAN_POINT('Origin',(0.115470053837925,0.,0.));
#23401=CARTESIAN_POINT('',(0.122286297108185,0.,-0.0118060796608386));
#23402=CARTESIAN_POINT('',(0.0577350269189626,-0.2,0.1));
#23403=CARTESIAN_POINT('Origin',(0.,-0.2,0.));
#23404=CARTESIAN_POINT('Origin',(0.17,0.,0.));
#23405=CARTESIAN_POINT('',(-0.17,-8.67361737988404E-18,-2.0818995585505E-17));
#23406=CARTESIAN_POINT('Origin',(0.,0.,0.));
#23407=CARTESIAN_POINT('Origin',(0.,-0.015,0.));
#23408=CARTESIAN_POINT('',(-0.1954,-0.0254,-2.39295984553393E-17));
#23409=CARTESIAN_POINT('Origin',(0.,-0.0254,0.));
#23410=CARTESIAN_POINT('',(-0.185,-0.015,-2.2655965784226E-17));
#23411=CARTESIAN_POINT('Origin',(0.,-0.2775,0.));
#23412=CARTESIAN_POINT('',(-0.1954,-0.5296,2.39295984553393E-17));
#23413=CARTESIAN_POINT('Origin',(0.,-0.5296,0.));
#23414=CARTESIAN_POINT('',(-0.1954,-0.2775,-2.39295984553393E-17));
#23415=CARTESIAN_POINT('Origin',(0.,-0.5625,0.));
#23416=CARTESIAN_POINT('',(-0.125,-0.6,-1.53080849893419E-17));
#23417=CARTESIAN_POINT('Origin',(0.,-0.6,0.));
#23418=CARTESIAN_POINT('',(-0.1625,-0.5625,-1.99005104861445E-17));
#23419=CARTESIAN_POINT('Origin',(0.,-0.6,0.));
#23521=UNCERTAINTY_MEASURE_WITH_UNIT(LENGTH_MEASURE(0.001),#23588,
'DISTANCE_ACCURACY_VALUE',
'Maximum model space distance between geometric entities at asserted c
onnectivities');
#23522=UNCERTAINTY_MEASURE_WITH_UNIT(LENGTH_MEASURE(0.001),#23588,
'DISTANCE_ACCURACY_VALUE',
'Maximum model space distance between geometric entities at asserted c
onnectivities');
#23586=(
GEOMETRIC_REPRESENTATION_CONTEXT(3)
GLOBAL_UNCERTAINTY_ASSIGNED_CONTEXT((#23521))
GLOBAL_UNIT_ASSIGNED_CONTEXT((#23588,#23590,#23591))
REPRESENTATION_CONTEXT('','3D')
);
#23587=(
GEOMETRIC_REPRESENTATION_CONTEXT(3)
GLOBAL_UNCERTAINTY_ASSIGNED_CONTEXT((#23522))
GLOBAL_UNIT_ASSIGNED_CONTEXT((#23588,#23590,#23591))
REPRESENTATION_CONTEXT('','3D')
);
#23588=(
LENGTH_UNIT()
NAMED_UNIT(*)
SI_UNIT(.CENTI.,.METRE.)
);
#23590=(
NAMED_UNIT(*)
PLANE_ANGLE_UNIT()
SI_UNIT($,.RADIAN.)
);
#23591=(
NAMED_UNIT(*)
SI_UNIT($,.STERADIAN.)
SOLID_ANGLE_UNIT()
);
#23655=SHAPE_DEFINITION_REPRESENTATION(#23786,#23888);
#23786=PRODUCT_DEFINITION_SHAPE('',$,#23953);
#23888=SHAPE_REPRESENTATION('',(#14462),#23586);
#23889=PRODUCT_DEFINITION_CONTEXT('part definition',#24083,'design');
#23953=PRODUCT_DEFINITION('Socket Set Screw - M4x6',
'Socket Set Screw - M4x6',#24017,#23889);
#24017=PRODUCT_DEFINITION_FORMATION('',$,#24148);
#24083=APPLICATION_CONTEXT(
'Core Data for Automotive Mechanical Design Process');
#24084=PRODUCT_CONTEXT('part definition',#24083,'mechanical');
#24148=PRODUCT('Socket Set Screw - M4x6','Socket Set Screw - M4x6',
'Socket Set Screw - M4x6',(#24084));
#24212=COLOUR_RGB('Black',0.12,0.14,0.17);
#24213=FILL_AREA_STYLE_COLOUR('',#24212);
#24214=FILL_AREA_STYLE('',(#24213));
#24215=SURFACE_STYLE_FILL_AREA(#24214);
#24216=SURFACE_SIDE_STYLE('',(#24215));
#24217=SURFACE_STYLE_USAGE(.BOTH.,#24216);
#24218=PRESENTATION_STYLE_ASSIGNMENT((#24217));
ENDSEC;
END-ISO-10303-21;
